ISO-10303-21;
HEADER;
/* Generated by software containing ST-Developer
 * from STEP Tools, Inc. (www.steptools.com) 
 */

FILE_DESCRIPTION(
/* description */ ('PAT-091'),
/* implementation_level */ '2;1');

FILE_NAME(
/* name */ 'Lead screw.step',
/* time_stamp */ '2026-10-27T15:34:44-07:00',
/* author */ (''),
/* organization */ (''),
/* preprocessor_version */ 'ST-DEVELOPER v20.2',
/* originating_system */ 'Autodesk Translation Framework v15.17.0.0',
/* authorisation */ '');

FILE_SCHEMA (('AUTOMOTIVE_DESIGN { 1 0 10303 214 3 1 1 }'));
ENDSEC;

DATA;
#10=MECHANICAL_DESIGN_GEOMETRIC_PRESENTATION_REPRESENTATION('',(#1088),#25100);
#855=SHAPE_REPRESENTATION_RELATIONSHIP('SRR','None',#25624,#965);
#965=ADVANCED_BREP_SHAPE_REPRESENTATION('',(#1209),#25094);
#1088=STYLED_ITEM('',(#26198),#1209);
#1209=MANIFOLD_SOLID_BREP('Body1',#13368);
#1625=FACE_BOUND('',#4077,.T.);
#1626=FACE_BOUND('',#4079,.T.);
#1627=FACE_BOUND('',#4083,.T.);
#1628=FACE_BOUND('',#4085,.T.);
#2046=PLANE('',#16384);
#2047=PLANE('',#16387);
#2048=PLANE('',#16393);
#2049=PLANE('',#16395);
#2050=PLANE('',#16403);
#2051=PLANE('',#16404);
#2848=FACE_OUTER_BOUND('',#4076,.T.);
#2849=FACE_OUTER_BOUND('',#4078,.T.);
#2850=FACE_OUTER_BOUND('',#4080,.T.);
#2851=FACE_OUTER_BOUND('',#4081,.T.);
#2852=FACE_OUTER_BOUND('',#4082,.T.);
#2853=FACE_OUTER_BOUND('',#4084,.T.);
#2854=FACE_OUTER_BOUND('',#4086,.T.);
#2855=FACE_OUTER_BOUND('',#4087,.T.);
#2856=FACE_OUTER_BOUND('',#4088,.T.);
#2857=FACE_OUTER_BOUND('',#4089,.T.);
#2858=FACE_OUTER_BOUND('',#4090,.T.);
#4076=EDGE_LOOP('',(#11978));
#4077=EDGE_LOOP('',(#11979));
#4078=EDGE_LOOP('',(#11980));
#4079=EDGE_LOOP('',(#11981));
#4080=EDGE_LOOP('',(#11982,#11983,#11984,#11985));
#4081=EDGE_LOOP('',(#11986,#11987,#11988,#11989));
#4082=EDGE_LOOP('',(#11990));
#4083=EDGE_LOOP('',(#11991));
#4084=EDGE_LOOP('',(#11992));
#4085=EDGE_LOOP('',(#11993));
#4086=EDGE_LOOP('',(#11994,#11995,#11996,#11997));
#4087=EDGE_LOOP('',(#11998,#11999,#12000,#12001));
#4088=EDGE_LOOP('',(#12002,#12003,#12004,#12005));
#4089=EDGE_LOOP('',(#12006));
#4090=EDGE_LOOP('',(#12007));
#4848=LINE('',#24738,#5588);
#4849=LINE('',#24741,#5589);
#4850=LINE('',#24752,#5590);
#4851=LINE('',#24755,#5591);
#4852=LINE('',#24760,#5592);
#5588=VECTOR('',#20804,0.8);
#5589=VECTOR('',#20807,0.6);
#5590=VECTOR('',#20822,0.8);
#5591=VECTOR('',#20825,0.6);
#5592=VECTOR('',#20832,0.6);
#6351=CIRCLE('',#16385,0.8);
#6352=CIRCLE('',#16386,0.6);
#6353=CIRCLE('',#16388,0.8);
#6354=CIRCLE('',#16389,0.6);
#6355=CIRCLE('',#16392,0.6);
#6356=CIRCLE('',#16394,0.8);
#6357=CIRCLE('',#16396,0.8);
#6358=CIRCLE('',#16397,0.6);
#6359=CIRCLE('',#16400,0.6);
#6360=CIRCLE('',#16402,0.6);
#7389=VERTEX_POINT('',#24728);
#7390=VERTEX_POINT('',#24730);
#7391=VERTEX_POINT('',#24733);
#7392=VERTEX_POINT('',#24735);
#7393=VERTEX_POINT('',#24740);
#7394=VERTEX_POINT('',#24744);
#7395=VERTEX_POINT('',#24747);
#7396=VERTEX_POINT('',#24749);
#7397=VERTEX_POINT('',#24754);
#7398=VERTEX_POINT('',#24758);
#8924=EDGE_CURVE('',#7389,#7389,#6351,.T.);
#8925=EDGE_CURVE('',#7390,#7390,#6352,.T.);
#8926=EDGE_CURVE('',#7391,#7391,#6353,.T.);
#8927=EDGE_CURVE('',#7392,#7392,#6354,.T.);
#8928=EDGE_CURVE('',#7389,#7391,#4848,.T.);
#8929=EDGE_CURVE('',#7392,#7393,#4849,.T.);
#8930=EDGE_CURVE('',#7393,#7393,#6355,.T.);
#8931=EDGE_CURVE('',#7394,#7394,#6356,.T.);
#8932=EDGE_CURVE('',#7395,#7395,#6357,.T.);
#8933=EDGE_CURVE('',#7396,#7396,#6358,.T.);
#8934=EDGE_CURVE('',#7394,#7395,#4850,.T.);
#8935=EDGE_CURVE('',#7396,#7397,#4851,.T.);
#8936=EDGE_CURVE('',#7397,#7397,#6359,.T.);
#8937=EDGE_CURVE('',#7398,#7398,#6360,.T.);
#8938=EDGE_CURVE('',#7398,#7390,#4852,.T.);
#11978=ORIENTED_EDGE('',*,*,#8924,.T.);
#11979=ORIENTED_EDGE('',*,*,#8925,.F.);
#11980=ORIENTED_EDGE('',*,*,#8926,.F.);
#11981=ORIENTED_EDGE('',*,*,#8927,.F.);
#11982=ORIENTED_EDGE('',*,*,#8924,.F.);
#11983=ORIENTED_EDGE('',*,*,#8928,.T.);
#11984=ORIENTED_EDGE('',*,*,#8926,.T.);
#11985=ORIENTED_EDGE('',*,*,#8928,.F.);
#11986=ORIENTED_EDGE('',*,*,#8927,.T.);
#11987=ORIENTED_EDGE('',*,*,#8929,.T.);
#11988=ORIENTED_EDGE('',*,*,#8930,.T.);
#11989=ORIENTED_EDGE('',*,*,#8929,.F.);
#11990=ORIENTED_EDGE('',*,*,#8931,.T.);
#11991=ORIENTED_EDGE('',*,*,#8930,.F.);
#11992=ORIENTED_EDGE('',*,*,#8932,.F.);
#11993=ORIENTED_EDGE('',*,*,#8933,.F.);
#11994=ORIENTED_EDGE('',*,*,#8931,.F.);
#11995=ORIENTED_EDGE('',*,*,#8934,.T.);
#11996=ORIENTED_EDGE('',*,*,#8932,.T.);
#11997=ORIENTED_EDGE('',*,*,#8934,.F.);
#11998=ORIENTED_EDGE('',*,*,#8933,.T.);
#11999=ORIENTED_EDGE('',*,*,#8935,.T.);
#12000=ORIENTED_EDGE('',*,*,#8936,.T.);
#12001=ORIENTED_EDGE('',*,*,#8935,.F.);
#12002=ORIENTED_EDGE('',*,*,#8937,.F.);
#12003=ORIENTED_EDGE('',*,*,#8938,.T.);
#12004=ORIENTED_EDGE('',*,*,#8925,.T.);
#12005=ORIENTED_EDGE('',*,*,#8938,.F.);
#12006=ORIENTED_EDGE('',*,*,#8937,.T.);
#12007=ORIENTED_EDGE('',*,*,#8936,.F.);
#12414=CYLINDRICAL_SURFACE('',#16390,0.8);
#12415=CYLINDRICAL_SURFACE('',#16391,0.6);
#12416=CYLINDRICAL_SURFACE('',#16398,0.8);
#12417=CYLINDRICAL_SURFACE('',#16399,0.6);
#12418=CYLINDRICAL_SURFACE('',#16401,0.6);
#13215=ADVANCED_FACE('',(#2848,#1625),#2046,.T.);
#13216=ADVANCED_FACE('',(#2849,#1626),#2047,.F.);
#13217=ADVANCED_FACE('',(#2850),#12414,.T.);
#13218=ADVANCED_FACE('',(#2851),#12415,.T.);
#13219=ADVANCED_FACE('',(#2852,#1627),#2048,.T.);
#13220=ADVANCED_FACE('',(#2853,#1628),#2049,.F.);
#13221=ADVANCED_FACE('',(#2854),#12416,.T.);
#13222=ADVANCED_FACE('',(#2855),#12417,.T.);
#13223=ADVANCED_FACE('',(#2856),#12418,.T.);
#13224=ADVANCED_FACE('',(#2857),#2050,.T.);
#13225=ADVANCED_FACE('',(#2858),#2051,.F.);
#13368=CLOSED_SHELL('',(#13215,#13216,#13217,#13218,#13219,#13220,#13221,
#13222,#13223,#13224,#13225));
#16383=AXIS2_PLACEMENT_3D('',#24726,#20788,#20789);
#16384=AXIS2_PLACEMENT_3D('',#24727,#20790,#20791);
#16385=AXIS2_PLACEMENT_3D('',#24729,#20792,#20793);
#16386=AXIS2_PLACEMENT_3D('',#24731,#20794,#20795);
#16387=AXIS2_PLACEMENT_3D('',#24732,#20796,#20797);
#16388=AXIS2_PLACEMENT_3D('',#24734,#20798,#20799);
#16389=AXIS2_PLACEMENT_3D('',#24736,#20800,#20801);
#16390=AXIS2_PLACEMENT_3D('',#24737,#20802,#20803);
#16391=AXIS2_PLACEMENT_3D('',#24739,#20805,#20806);
#16392=AXIS2_PLACEMENT_3D('',#24742,#20808,#20809);
#16393=AXIS2_PLACEMENT_3D('',#24743,#20810,#20811);
#16394=AXIS2_PLACEMENT_3D('',#24745,#20812,#20813);
#16395=AXIS2_PLACEMENT_3D('',#24746,#20814,#20815);
#16396=AXIS2_PLACEMENT_3D('',#24748,#20816,#20817);
#16397=AXIS2_PLACEMENT_3D('',#24750,#20818,#20819);
#16398=AXIS2_PLACEMENT_3D('',#24751,#20820,#20821);
#16399=AXIS2_PLACEMENT_3D('',#24753,#20823,#20824);
#16400=AXIS2_PLACEMENT_3D('',#24756,#20826,#20827);
#16401=AXIS2_PLACEMENT_3D('',#24757,#20828,#20829);
#16402=AXIS2_PLACEMENT_3D('',#24759,#20830,#20831);
#16403=AXIS2_PLACEMENT_3D('',#24761,#20833,#20834);
#16404=AXIS2_PLACEMENT_3D('',#24762,#20835,#20836);
#20788=DIRECTION('axis',(0.,0.,1.));
#20789=DIRECTION('refdir',(1.,0.,0.));
#20790=DIRECTION('center_axis',(1.,0.,0.));
#20791=DIRECTION('ref_axis',(0.,0.,-1.));
#20792=DIRECTION('center_axis',(1.,0.,0.));
#20793=DIRECTION('ref_axis',(0.,0.,-1.));
#20794=DIRECTION('center_axis',(1.,0.,0.));
#20795=DIRECTION('ref_axis',(0.,0.,-1.));
#20796=DIRECTION('center_axis',(1.,0.,0.));
#20797=DIRECTION('ref_axis',(0.,0.,-1.));
#20798=DIRECTION('center_axis',(1.,0.,0.));
#20799=DIRECTION('ref_axis',(0.,0.,-1.));
#20800=DIRECTION('center_axis',(-1.,0.,0.));
#20801=DIRECTION('ref_axis',(0.,0.,-1.));
#20802=DIRECTION('center_axis',(1.,0.,0.));
#20803=DIRECTION('ref_axis',(0.,0.,-1.));
#20804=DIRECTION('',(-1.,0.,0.));
#20805=DIRECTION('center_axis',(1.,0.,0.));
#20806=DIRECTION('ref_axis',(0.,0.,-1.));
#20807=DIRECTION('',(-1.,0.,0.));
#20808=DIRECTION('center_axis',(1.,0.,0.));
#20809=DIRECTION('ref_axis',(0.,0.,-1.));
#20810=DIRECTION('center_axis',(1.,0.,0.));
#20811=DIRECTION('ref_axis',(0.,0.,-1.));
#20812=DIRECTION('center_axis',(1.,0.,0.));
#20813=DIRECTION('ref_axis',(0.,0.,-1.));
#20814=DIRECTION('center_axis',(1.,0.,0.));
#20815=DIRECTION('ref_axis',(0.,0.,-1.));
#20816=DIRECTION('center_axis',(1.,0.,0.));
#20817=DIRECTION('ref_axis',(0.,0.,-1.));
#20818=DIRECTION('center_axis',(-1.,0.,0.));
#20819=DIRECTION('ref_axis',(0.,0.,-1.));
#20820=DIRECTION('center_axis',(1.,0.,0.));
#20821=DIRECTION('ref_axis',(0.,0.,-1.));
#20822=DIRECTION('',(-1.,0.,0.));
#20823=DIRECTION('center_axis',(1.,0.,0.));
#20824=DIRECTION('ref_axis',(0.,0.,-1.));
#20825=DIRECTION('',(-1.,0.,0.));
#20826=DIRECTION('center_axis',(1.,0.,0.));
#20827=DIRECTION('ref_axis',(0.,0.,-1.));
#20828=DIRECTION('center_axis',(1.,0.,0.));
#20829=DIRECTION('ref_axis',(0.,0.,-1.));
#20830=DIRECTION('center_axis',(1.,0.,0.));
#20831=DIRECTION('ref_axis',(0.,0.,-1.));
#20832=DIRECTION('',(-1.,0.,0.));
#20833=DIRECTION('center_axis',(1.,0.,0.));
#20834=DIRECTION('ref_axis',(0.,0.,-1.));
#20835=DIRECTION('center_axis',(1.,0.,0.));
#20836=DIRECTION('ref_axis',(0.,0.,-1.));
#24726=CARTESIAN_POINT('',(0.,0.,0.));
#24727=CARTESIAN_POINT('Origin',(44.5,0.,6.));
#24728=CARTESIAN_POINT('',(44.5,-9.79717439317882E-17,6.8));
#24729=CARTESIAN_POINT('Origin',(44.5,0.,6.));
#24730=CARTESIAN_POINT('',(44.5,-7.34788079488412E-17,6.6));
#24731=CARTESIAN_POINT('Origin',(44.5,0.,6.));
#24732=CARTESIAN_POINT('Origin',(44.,0.,6.));
#24733=CARTESIAN_POINT('',(44.,-9.79717439317882E-17,6.8));
#24734=CARTESIAN_POINT('Origin',(44.,0.,6.));
#24735=CARTESIAN_POINT('',(44.,7.34788079488412E-17,6.6));
#24736=CARTESIAN_POINT('Origin',(44.,0.,6.));
#24737=CARTESIAN_POINT('Origin',(44.,0.,6.));
#24738=CARTESIAN_POINT('',(44.,-9.79717439317882E-17,6.8));
#24739=CARTESIAN_POINT('Origin',(-3.5,0.,6.));
#24740=CARTESIAN_POINT('',(1.,-7.34788079488412E-17,6.6));
#24741=CARTESIAN_POINT('',(-3.5,-7.34788079488412E-17,6.6));
#24742=CARTESIAN_POINT('Origin',(1.,0.,6.));
#24743=CARTESIAN_POINT('Origin',(1.,0.,6.));
#24744=CARTESIAN_POINT('',(1.,-9.79717439317882E-17,6.8));
#24745=CARTESIAN_POINT('Origin',(1.,0.,6.));
#24746=CARTESIAN_POINT('Origin',(0.5,0.,6.));
#24747=CARTESIAN_POINT('',(0.5,-9.79717439317882E-17,6.8));
#24748=CARTESIAN_POINT('Origin',(0.5,0.,6.));
#24749=CARTESIAN_POINT('',(0.5,7.34788079488412E-17,6.6));
#24750=CARTESIAN_POINT('Origin',(0.5,0.,6.));
#24751=CARTESIAN_POINT('Origin',(0.5,0.,6.));
#24752=CARTESIAN_POINT('',(0.5,-9.79717439317882E-17,6.8));
#24753=CARTESIAN_POINT('Origin',(-3.5,0.,6.));
#24754=CARTESIAN_POINT('',(-3.5,-7.34788079488412E-17,6.6));
#24755=CARTESIAN_POINT('',(-3.5,-7.34788079488412E-17,6.6));
#24756=CARTESIAN_POINT('Origin',(-3.5,0.,6.));
#24757=CARTESIAN_POINT('Origin',(-3.5,0.,6.));
#24758=CARTESIAN_POINT('',(47.,-7.34788079488412E-17,6.6));
#24759=CARTESIAN_POINT('Origin',(47.,0.,6.));
#24760=CARTESIAN_POINT('',(-3.5,-7.34788079488412E-17,6.6));
#24761=CARTESIAN_POINT('Origin',(47.,0.,6.));
#24762=CARTESIAN_POINT('Origin',(-3.5,0.,6.));
#24973=UNCERTAINTY_MEASURE_WITH_UNIT(LENGTH_MEASURE(0.001),#25101,
'DISTANCE_ACCURACY_VALUE',
'Maximum model space distance between geometric entities at asserted c
onnectivities');
#24979=UNCERTAINTY_MEASURE_WITH_UNIT(LENGTH_MEASURE(0.001),#25101,
'DISTANCE_ACCURACY_VALUE',
'Maximum model space distance between geometric entities at asserted c
onnectivities');
#25094=(
GEOMETRIC_REPRESENTATION_CONTEXT(3)
GLOBAL_UNCERTAINTY_ASSIGNED_CONTEXT((#24973))
GLOBAL_UNIT_ASSIGNED_CONTEXT((#25101,#25103,#25104))
REPRESENTATION_CONTEXT('','3D')
);
#25100=(
GEOMETRIC_REPRESENTATION_CONTEXT(3)
GLOBAL_UNCERTAINTY_ASSIGNED_CONTEXT((#24979))
GLOBAL_UNIT_ASSIGNED_CONTEXT((#25101,#25103,#25104))
REPRESENTATION_CONTEXT('','3D')
);
#25101=(
LENGTH_UNIT()
NAMED_UNIT(*)
SI_UNIT(.CENTI.,.METRE.)
);
#25103=(
NAMED_UNIT(*)
PLANE_ANGLE_UNIT()
SI_UNIT($,.RADIAN.)
);
#25104=(
NAMED_UNIT(*)
SI_UNIT($,.STERADIAN.)
SOLID_ANGLE_UNIT()
);
#25219=SHAPE_DEFINITION_REPRESENTATION(#25491,#25624);
#25491=PRODUCT_DEFINITION_SHAPE('',$,#25745);
#25624=SHAPE_REPRESENTATION('',(#16383),#25094);
#25630=PRODUCT_DEFINITION_CONTEXT('part definition',#25992,'design');
#25745=PRODUCT_DEFINITION('Lead screw','Lead screw',#25865,#25630);
#25865=PRODUCT_DEFINITION_FORMATION('',$,#26108);
#25992=APPLICATION_CONTEXT(
'Core Data for Automotive Mechanical Design Process');
#25993=PRODUCT_CONTEXT('part definition',#25992,'mechanical');
#26108=PRODUCT('Lead screw','Lead screw','Lead screw',(#25993));
#26192=COLOUR_RGB('Black',0.12,0.14,0.17);
#26193=FILL_AREA_STYLE_COLOUR('',#26192);
#26194=FILL_AREA_STYLE('',(#26193));
#26195=SURFACE_STYLE_FILL_AREA(#26194);
#26196=SURFACE_SIDE_STYLE('',(#26195));
#26197=SURFACE_STYLE_USAGE(.BOTH.,#26196);
#26198=PRESENTATION_STYLE_ASSIGNMENT((#26197));
ENDSEC;
END-ISO-10303-21;
